ISO-10303-21;
HEADER;
/* Generated by software containing ST-Developer
 * from STEP Tools, Inc. (www.steptools.com) 
 */

FILE_DESCRIPTION(
/* description */ ('Gear mesh backlash fixture'),
/* implementation_level */ '2;1');

FILE_NAME(
/* name */ 'M4x10 Cap Screw.step',
/* time_stamp */ '2026-10-28T03:26:00-07:00',
/* author */ (''),
/* organization */ (''),
/* preprocessor_version */ 'ST-DEVELOPER v20.2',
/* originating_system */ 'Autodesk Translation Framework v15.17.0.0',
/* authorisation */ '');

FILE_SCHEMA (('AUTOMOTIVE_DESIGN { 1 0 10303 214 3 1 1 }'));
ENDSEC;

DATA;
#10=MECHANICAL_DESIGN_GEOMETRIC_PRESENTATION_REPRESENTATION('',(#1080),#57900);
#373=ORIENTED_CLOSED_SHELL('',*,#13642,.F.);
#376=BREP_WITH_VOIDS('Body1',#13643,(#373));
#777=CONICAL_SURFACE('',#15492,0.325,0.785398163397448);
#778=CONICAL_SURFACE('',#15496,0.335,0.785398163397448);
#779=CONICAL_SURFACE('',#15500,0.21,0.463647609000806);
#965=SHAPE_REPRESENTATION_RELATIONSHIP('SRR','None',#58166,#1015);
#1015=ADVANCED_BREP_SHAPE_REPRESENTATION('',(#376),#57899);
#1080=STYLED_ITEM('',(#58472),#376);
#1329=FACE_BOUND('',#3408,.T.);
#1683=PLANE('',#15480);
#1684=PLANE('',#15481);
#1685=PLANE('',#15482);
#1686=PLANE('',#15483);
#1687=PLANE('',#15484);
#1688=PLANE('',#15485);
#1689=PLANE('',#15486);
#1690=PLANE('',#15487);
#1691=PLANE('',#15488);
#1692=PLANE('',#15490);
#1693=PLANE('',#15498);
#2443=FACE_OUTER_BOUND('',#3394,.T.);
#2444=FACE_OUTER_BOUND('',#3395,.T.);
#2445=FACE_OUTER_BOUND('',#3396,.T.);
#2446=FACE_OUTER_BOUND('',#3397,.T.);
#2447=FACE_OUTER_BOUND('',#3398,.T.);
#2448=FACE_OUTER_BOUND('',#3399,.T.);
#2449=FACE_OUTER_BOUND('',#3400,.T.);
#2450=FACE_OUTER_BOUND('',#3401,.T.);
#2451=FACE_OUTER_BOUND('',#3402,.T.);
#2452=FACE_OUTER_BOUND('',#3403,.T.);
#2453=FACE_OUTER_BOUND('',#3404,.T.);
#2454=FACE_OUTER_BOUND('',#3405,.T.);
#2455=FACE_OUTER_BOUND('',#3406,.T.);
#2456=FACE_OUTER_BOUND('',#3407,.T.);
#2457=FACE_OUTER_BOUND('',#3409,.T.);
#2458=FACE_OUTER_BOUND('',#3410,.T.);
#3394=EDGE_LOOP('',(#12525,#12526,#12527,#12528));
#3395=EDGE_LOOP('',(#12529,#12530,#12531,#12532));
#3396=EDGE_LOOP('',(#12533,#12534,#12535,#12536));
#3397=EDGE_LOOP('',(#12537,#12538,#12539,#12540));
#3398=EDGE_LOOP('',(#12541,#12542,#12543,#12544));
#3399=EDGE_LOOP('',(#12545,#12546,#12547,#12548));
#3400=EDGE_LOOP('',(#12549,#12550,#12551,#12552,#12553,#12554));
#3401=EDGE_LOOP('',(#12555,#12556,#12557,#12558,#12559,#12560));
#3402=EDGE_LOOP('',(#12561));
#3403=EDGE_LOOP('',(#12562));
#3404=EDGE_LOOP('',(#12563,#12564,#12565,#12566));
#3405=EDGE_LOOP('',(#12567,#12568,#12569,#12570));
#3406=EDGE_LOOP('',(#12571,#12572,#12573,#12574));
#3407=EDGE_LOOP('',(#12575));
#3408=EDGE_LOOP('',(#12576));
#3409=EDGE_LOOP('',(#12577,#12578,#12579,#12580));
#3410=EDGE_LOOP('',(#12581,#12582,#12583,#12584));
#4277=LINE('',#57646,#5166);
#4278=LINE('',#57648,#5167);
#4279=LINE('',#57650,#5168);
#4280=LINE('',#57651,#5169);
#4281=LINE('',#57654,#5170);
#4282=LINE('',#57656,#5171);
#4283=LINE('',#57657,#5172);
#4284=LINE('',#57660,#5173);
#4285=LINE('',#57662,#5174);
#4286=LINE('',#57663,#5175);
#4287=LINE('',#57666,#5176);
#4288=LINE('',#57668,#5177);
#4289=LINE('',#57669,#5178);
#4290=LINE('',#57672,#5179);
#4291=LINE('',#57674,#5180);
#4292=LINE('',#57675,#5181);
#4293=LINE('',#57677,#5182);
#4294=LINE('',#57678,#5183);
#4295=LINE('',#57690,#5184);
#4296=LINE('',#57694,#5185);
#4297=LINE('',#57698,#5186);
#4298=LINE('',#57705,#5187);
#4299=LINE('',#57707,#5188);
#5166=VECTOR('',#19016,1.);
#5167=VECTOR('',#19017,1.);
#5168=VECTOR('',#19018,1.);
#5169=VECTOR('',#19019,1.);
#5170=VECTOR('',#19022,1.);
#5171=VECTOR('',#19023,1.);
#5172=VECTOR('',#19024,1.);
#5173=VECTOR('',#19027,1.);
#5174=VECTOR('',#19028,1.);
#5175=VECTOR('',#19029,1.);
#5176=VECTOR('',#19032,1.);
#5177=VECTOR('',#19033,1.);
#5178=VECTOR('',#19034,1.);
#5179=VECTOR('',#19037,1.);
#5180=VECTOR('',#19038,1.);
#5181=VECTOR('',#19039,1.);
#5182=VECTOR('',#19042,1.);
#5183=VECTOR('',#19043,1.);
#5184=VECTOR('',#19060,0.325);
#5185=VECTOR('',#19065,0.35);
#5186=VECTOR('',#19070,0.335);
#5187=VECTOR('',#19079,0.21);
#5188=VECTOR('',#19082,0.2);
#5774=CIRCLE('',#15489,0.1954);
#5775=CIRCLE('',#15491,0.3);
#5776=CIRCLE('',#15493,0.35);
#5777=CIRCLE('',#15495,0.35);
#5778=CIRCLE('',#15497,0.32);
#5779=CIRCLE('',#15499,0.22);
#5780=CIRCLE('',#15501,0.1954);
#7007=VERTEX_POINT('',#57644);
#7008=VERTEX_POINT('',#57645);
#7009=VERTEX_POINT('',#57647);
#7010=VERTEX_POINT('',#57649);
#7011=VERTEX_POINT('',#57653);
#7012=VERTEX_POINT('',#57655);
#7013=VERTEX_POINT('',#57659);
#7014=VERTEX_POINT('',#57661);
#7015=VERTEX_POINT('',#57665);
#7016=VERTEX_POINT('',#57667);
#7017=VERTEX_POINT('',#57671);
#7018=VERTEX_POINT('',#57673);
#7019=VERTEX_POINT('',#57682);
#7020=VERTEX_POINT('',#57685);
#7021=VERTEX_POINT('',#57688);
#7022=VERTEX_POINT('',#57692);
#7023=VERTEX_POINT('',#57696);
#7024=VERTEX_POINT('',#57700);
#7025=VERTEX_POINT('',#57703);
#8849=EDGE_CURVE('',#7007,#7008,#4277,.T.);
#8850=EDGE_CURVE('',#7008,#7009,#4278,.T.);
#8851=EDGE_CURVE('',#7009,#7010,#4279,.T.);
#8852=EDGE_CURVE('',#7007,#7010,#4280,.T.);
#8853=EDGE_CURVE('',#7008,#7011,#4281,.T.);
#8854=EDGE_CURVE('',#7011,#7012,#4282,.T.);
#8855=EDGE_CURVE('',#7012,#7009,#4283,.T.);
#8856=EDGE_CURVE('',#7011,#7013,#4284,.T.);
#8857=EDGE_CURVE('',#7013,#7014,#4285,.T.);
#8858=EDGE_CURVE('',#7014,#7012,#4286,.T.);
#8859=EDGE_CURVE('',#7013,#7015,#4287,.T.);
#8860=EDGE_CURVE('',#7015,#7016,#4288,.T.);
#8861=EDGE_CURVE('',#7016,#7014,#4289,.T.);
#8862=EDGE_CURVE('',#7015,#7017,#4290,.T.);
#8863=EDGE_CURVE('',#7017,#7018,#4291,.T.);
#8864=EDGE_CURVE('',#7018,#7016,#4292,.T.);
#8865=EDGE_CURVE('',#7017,#7007,#4293,.T.);
#8866=EDGE_CURVE('',#7010,#7018,#4294,.T.);
#8867=EDGE_CURVE('',#7019,#7019,#5774,.T.);
#8868=EDGE_CURVE('',#7020,#7020,#5775,.T.);
#8869=EDGE_CURVE('',#7021,#7021,#5776,.T.);
#8870=EDGE_CURVE('',#7021,#7020,#4295,.T.);
#8871=EDGE_CURVE('',#7022,#7022,#5777,.T.);
#8872=EDGE_CURVE('',#7022,#7021,#4296,.T.);
#8873=EDGE_CURVE('',#7023,#7023,#5778,.T.);
#8874=EDGE_CURVE('',#7023,#7022,#4297,.T.);
#8875=EDGE_CURVE('',#7024,#7024,#5779,.T.);
#8876=EDGE_CURVE('',#7025,#7025,#5780,.F.);
#8877=EDGE_CURVE('',#7025,#7024,#4298,.T.);
#8878=EDGE_CURVE('',#7019,#7025,#4299,.T.);
#12525=ORIENTED_EDGE('',*,*,#8849,.T.);
#12526=ORIENTED_EDGE('',*,*,#8850,.T.);
#12527=ORIENTED_EDGE('',*,*,#8851,.T.);
#12528=ORIENTED_EDGE('',*,*,#8852,.F.);
#12529=ORIENTED_EDGE('',*,*,#8853,.T.);
#12530=ORIENTED_EDGE('',*,*,#8854,.T.);
#12531=ORIENTED_EDGE('',*,*,#8855,.T.);
#12532=ORIENTED_EDGE('',*,*,#8850,.F.);
#12533=ORIENTED_EDGE('',*,*,#8856,.T.);
#12534=ORIENTED_EDGE('',*,*,#8857,.T.);
#12535=ORIENTED_EDGE('',*,*,#8858,.T.);
#12536=ORIENTED_EDGE('',*,*,#8854,.F.);
#12537=ORIENTED_EDGE('',*,*,#8859,.T.);
#12538=ORIENTED_EDGE('',*,*,#8860,.T.);
#12539=ORIENTED_EDGE('',*,*,#8861,.T.);
#12540=ORIENTED_EDGE('',*,*,#8857,.F.);
#12541=ORIENTED_EDGE('',*,*,#8862,.T.);
#12542=ORIENTED_EDGE('',*,*,#8863,.T.);
#12543=ORIENTED_EDGE('',*,*,#8864,.T.);
#12544=ORIENTED_EDGE('',*,*,#8860,.F.);
#12545=ORIENTED_EDGE('',*,*,#8865,.T.);
#12546=ORIENTED_EDGE('',*,*,#8852,.T.);
#12547=ORIENTED_EDGE('',*,*,#8866,.T.);
#12548=ORIENTED_EDGE('',*,*,#8863,.F.);
#12549=ORIENTED_EDGE('',*,*,#8865,.F.);
#12550=ORIENTED_EDGE('',*,*,#8862,.F.);
#12551=ORIENTED_EDGE('',*,*,#8859,.F.);
#12552=ORIENTED_EDGE('',*,*,#8856,.F.);
#12553=ORIENTED_EDGE('',*,*,#8853,.F.);
#12554=ORIENTED_EDGE('',*,*,#8849,.F.);
#12555=ORIENTED_EDGE('',*,*,#8866,.F.);
#12556=ORIENTED_EDGE('',*,*,#8851,.F.);
#12557=ORIENTED_EDGE('',*,*,#8855,.F.);
#12558=ORIENTED_EDGE('',*,*,#8858,.F.);
#12559=ORIENTED_EDGE('',*,*,#8861,.F.);
#12560=ORIENTED_EDGE('',*,*,#8864,.F.);
#12561=ORIENTED_EDGE('',*,*,#8867,.F.);
#12562=ORIENTED_EDGE('',*,*,#8868,.F.);
#12563=ORIENTED_EDGE('',*,*,#8869,.F.);
#12564=ORIENTED_EDGE('',*,*,#8870,.T.);
#12565=ORIENTED_EDGE('',*,*,#8868,.T.);
#12566=ORIENTED_EDGE('',*,*,#8870,.F.);
#12567=ORIENTED_EDGE('',*,*,#8871,.F.);
#12568=ORIENTED_EDGE('',*,*,#8872,.T.);
#12569=ORIENTED_EDGE('',*,*,#8869,.T.);
#12570=ORIENTED_EDGE('',*,*,#8872,.F.);
#12571=ORIENTED_EDGE('',*,*,#8873,.F.);
#12572=ORIENTED_EDGE('',*,*,#8874,.T.);
#12573=ORIENTED_EDGE('',*,*,#8871,.T.);
#12574=ORIENTED_EDGE('',*,*,#8874,.F.);
#12575=ORIENTED_EDGE('',*,*,#8873,.T.);
#12576=ORIENTED_EDGE('',*,*,#8875,.F.);
#12577=ORIENTED_EDGE('',*,*,#8876,.F.);
#12578=ORIENTED_EDGE('',*,*,#8877,.T.);
#12579=ORIENTED_EDGE('',*,*,#8875,.T.);
#12580=ORIENTED_EDGE('',*,*,#8877,.F.);
#12581=ORIENTED_EDGE('',*,*,#8867,.T.);
#12582=ORIENTED_EDGE('',*,*,#8878,.T.);
#12583=ORIENTED_EDGE('',*,*,#8876,.T.);
#12584=ORIENTED_EDGE('',*,*,#8878,.F.);
#12809=CYLINDRICAL_SURFACE('',#15494,0.35);
#12810=CYLINDRICAL_SURFACE('',#15502,0.1954);
#13560=ADVANCED_FACE('',(#2443),#1683,.F.);
#13561=ADVANCED_FACE('',(#2444),#1684,.F.);
#13562=ADVANCED_FACE('',(#2445),#1685,.F.);
#13563=ADVANCED_FACE('',(#2446),#1686,.F.);
#13564=ADVANCED_FACE('',(#2447),#1687,.F.);
#13565=ADVANCED_FACE('',(#2448),#1688,.F.);
#13566=ADVANCED_FACE('',(#2449),#1689,.F.);
#13567=ADVANCED_FACE('',(#2450),#1690,.F.);
#13568=ADVANCED_FACE('',(#2451),#1691,.F.);
#13569=ADVANCED_FACE('',(#2452),#1692,.T.);
#13570=ADVANCED_FACE('',(#2453),#777,.T.);
#13571=ADVANCED_FACE('',(#2454),#12809,.T.);
#13572=ADVANCED_FACE('',(#2455),#778,.T.);
#13573=ADVANCED_FACE('',(#2456,#1329),#1693,.T.);
#13574=ADVANCED_FACE('',(#2457),#779,.T.);
#13575=ADVANCED_FACE('',(#2458),#12810,.T.);
#13642=CLOSED_SHELL('',(#13560,#13561,#13562,#13563,#13564,#13565,#13566,
#13567));
#13643=CLOSED_SHELL('',(#13568,#13569,#13570,#13571,#13572,#13573,#13574,
#13575));
#15479=AXIS2_PLACEMENT_3D('',#57642,#19012,#19013);
#15480=AXIS2_PLACEMENT_3D('',#57643,#19014,#19015);
#15481=AXIS2_PLACEMENT_3D('',#57652,#19020,#19021);
#15482=AXIS2_PLACEMENT_3D('',#57658,#19025,#19026);
#15483=AXIS2_PLACEMENT_3D('',#57664,#19030,#19031);
#15484=AXIS2_PLACEMENT_3D('',#57670,#19035,#19036);
#15485=AXIS2_PLACEMENT_3D('',#57676,#19040,#19041);
#15486=AXIS2_PLACEMENT_3D('',#57679,#19044,#19045);
#15487=AXIS2_PLACEMENT_3D('',#57680,#19046,#19047);
#15488=AXIS2_PLACEMENT_3D('',#57681,#19048,#19049);
#15489=AXIS2_PLACEMENT_3D('',#57683,#19050,#19051);
#15490=AXIS2_PLACEMENT_3D('',#57684,#19052,#19053);
#15491=AXIS2_PLACEMENT_3D('',#57686,#19054,#19055);
#15492=AXIS2_PLACEMENT_3D('',#57687,#19056,#19057);
#15493=AXIS2_PLACEMENT_3D('',#57689,#19058,#19059);
#15494=AXIS2_PLACEMENT_3D('',#57691,#19061,#19062);
#15495=AXIS2_PLACEMENT_3D('',#57693,#19063,#19064);
#15496=AXIS2_PLACEMENT_3D('',#57695,#19066,#19067);
#15497=AXIS2_PLACEMENT_3D('',#57697,#19068,#19069);
#15498=AXIS2_PLACEMENT_3D('',#57699,#19071,#19072);
#15499=AXIS2_PLACEMENT_3D('',#57701,#19073,#19074);
#15500=AXIS2_PLACEMENT_3D('',#57702,#19075,#19076);
#15501=AXIS2_PLACEMENT_3D('',#57704,#19077,#19078);
#15502=AXIS2_PLACEMENT_3D('',#57706,#19080,#19081);
#19012=DIRECTION('axis',(0.,0.,1.));
#19013=DIRECTION('refdir',(1.,0.,0.));
#19014=DIRECTION('center_axis',(0.866025403784439,0.,-0.5));
#19015=DIRECTION('ref_axis',(0.5,0.,0.866025403784439));
#19016=DIRECTION('',(-0.5,0.,-0.866025403784439));
#19017=DIRECTION('',(0.,-1.,0.));
#19018=DIRECTION('',(0.5,0.,0.866025403784439));
#19019=DIRECTION('',(0.,-1.,0.));
#19020=DIRECTION('center_axis',(1.60246890531964E-16,0.,-1.));
#19021=DIRECTION('ref_axis',(1.,0.,1.60246890531964E-16));
#19022=DIRECTION('',(-1.,0.,-1.60246890531964E-16));
#19023=DIRECTION('',(0.,-1.,0.));
#19024=DIRECTION('',(1.,0.,1.60246890531964E-16));
#19025=DIRECTION('center_axis',(-0.866025403784439,0.,-0.5));
#19026=DIRECTION('ref_axis',(0.5,0.,-0.866025403784439));
#19027=DIRECTION('',(-0.5,0.,0.866025403784439));
#19028=DIRECTION('',(0.,-1.,0.));
#19029=DIRECTION('',(0.5,0.,-0.866025403784439));
#19030=DIRECTION('center_axis',(-0.866025403784439,0.,0.5));
#19031=DIRECTION('ref_axis',(-0.5,0.,-0.866025403784439));
#19032=DIRECTION('',(0.5,0.,0.866025403784439));
#19033=DIRECTION('',(0.,-1.,0.));
#19034=DIRECTION('',(-0.5,0.,-0.866025403784439));
#19035=DIRECTION('center_axis',(-1.60246890531964E-16,0.,1.));
#19036=DIRECTION('ref_axis',(-1.,0.,-1.60246890531964E-16));
#19037=DIRECTION('',(1.,0.,1.60246890531964E-16));
#19038=DIRECTION('',(0.,-1.,0.));
#19039=DIRECTION('',(-1.,0.,-1.60246890531964E-16));
#19040=DIRECTION('center_axis',(0.866025403784439,0.,0.5));
#19041=DIRECTION('ref_axis',(-0.5,0.,0.866025403784439));
#19042=DIRECTION('',(0.5,0.,-0.866025403784439));
#19043=DIRECTION('',(-0.5,0.,0.866025403784439));
#19044=DIRECTION('center_axis',(0.,1.,0.));
#19045=DIRECTION('ref_axis',(1.,0.,0.));
#19046=DIRECTION('center_axis',(0.,-1.,0.));
#19047=DIRECTION('ref_axis',(0.,0.,-1.));
#19048=DIRECTION('center_axis',(0.,1.,0.));
#19049=DIRECTION('ref_axis',(1.,0.,0.));
#19050=DIRECTION('center_axis',(0.,1.,0.));
#19051=DIRECTION('ref_axis',(1.,0.,0.));
#19052=DIRECTION('center_axis',(0.,1.,0.));
#19053=DIRECTION('ref_axis',(0.,0.,1.));
#19054=DIRECTION('center_axis',(0.,-1.,0.));
#19055=DIRECTION('ref_axis',(1.,0.,0.));
#19056=DIRECTION('center_axis',(0.,-1.,0.));
#19057=DIRECTION('ref_axis',(1.,0.,0.));
#19058=DIRECTION('center_axis',(0.,-1.,0.));
#19059=DIRECTION('ref_axis',(1.,0.,0.));
#19060=DIRECTION('',(0.707106781186547,0.707106781186548,8.65956056235493E-17));
#19061=DIRECTION('center_axis',(0.,-1.,0.));
#19062=DIRECTION('ref_axis',(1.,0.,0.));
#19063=DIRECTION('center_axis',(0.,-1.,0.));
#19064=DIRECTION('ref_axis',(1.,0.,0.));
#19065=DIRECTION('',(0.,1.,0.));
#19066=DIRECTION('center_axis',(0.,1.,0.));
#19067=DIRECTION('ref_axis',(1.,0.,0.));
#19068=DIRECTION('center_axis',(0.,-1.,0.));
#19069=DIRECTION('ref_axis',(1.,0.,0.));
#19070=DIRECTION('',(-0.707106781186547,0.707106781186548,-8.65956056235493E-17));
#19071=DIRECTION('center_axis',(0.,-1.,0.));
#19072=DIRECTION('ref_axis',(0.,0.,-1.));
#19073=DIRECTION('center_axis',(0.,-1.,0.));
#19074=DIRECTION('ref_axis',(1.,0.,0.));
#19075=DIRECTION('center_axis',(0.,1.,0.));
#19076=DIRECTION('ref_axis',(1.,0.,0.));
#19077=DIRECTION('center_axis',(0.,1.,0.));
#19078=DIRECTION('ref_axis',(1.,0.,0.));
#19079=DIRECTION('',(-0.447213595499958,0.894427190999916,-5.47678698264203E-17));
#19080=DIRECTION('center_axis',(0.,-1.,0.));
#19081=DIRECTION('ref_axis',(1.,0.,0.));
#19082=DIRECTION('',(0.,1.,0.));
#57642=CARTESIAN_POINT('',(0.,0.,0.));
#57643=CARTESIAN_POINT('Origin',(0.0866025403784439,-0.4,-0.15));
#57644=CARTESIAN_POINT('',(0.173205080756888,-0.4,0.));
#57645=CARTESIAN_POINT('',(0.0866025403784439,-0.4,-0.15));
#57646=CARTESIAN_POINT('',(0.173205080756888,-0.4,0.));
#57647=CARTESIAN_POINT('',(0.0866025403784439,-0.64,-0.15));
#57648=CARTESIAN_POINT('',(0.0866025403784439,-0.4,-0.15));
#57649=CARTESIAN_POINT('',(0.173205080756888,-0.64,0.));
#57650=CARTESIAN_POINT('',(0.173205080756888,-0.64,0.));
#57651=CARTESIAN_POINT('',(0.173205080756888,-0.4,0.));
#57652=CARTESIAN_POINT('Origin',(-0.0866025403784438,-0.4,-0.15));
#57653=CARTESIAN_POINT('',(-0.0866025403784438,-0.4,-0.15));
#57654=CARTESIAN_POINT('',(0.0866025403784439,-0.4,-0.15));
#57655=CARTESIAN_POINT('',(-0.0866025403784438,-0.64,-0.15));
#57656=CARTESIAN_POINT('',(-0.0866025403784438,-0.4,-0.15));
#57657=CARTESIAN_POINT('',(0.0866025403784439,-0.64,-0.15));
#57658=CARTESIAN_POINT('Origin',(-0.173205080756888,-0.4,-2.77555756156289E-17));
#57659=CARTESIAN_POINT('',(-0.173205080756888,-0.4,-2.12115047744981E-17));
#57660=CARTESIAN_POINT('',(-0.0866025403784438,-0.4,-0.15));
#57661=CARTESIAN_POINT('',(-0.173205080756888,-0.64,-2.77555756156289E-17));
#57662=CARTESIAN_POINT('',(-0.173205080756888,-0.4,-2.12115047744981E-17));
#57663=CARTESIAN_POINT('',(-0.0866025403784438,-0.64,-0.15));
#57664=CARTESIAN_POINT('Origin',(-0.0866025403784439,-0.4,0.15));
#57665=CARTESIAN_POINT('',(-0.0866025403784439,-0.4,0.15));
#57666=CARTESIAN_POINT('',(-0.173205080756888,-0.4,-2.12115047744981E-17));
#57667=CARTESIAN_POINT('',(-0.0866025403784439,-0.64,0.15));
#57668=CARTESIAN_POINT('',(-0.0866025403784439,-0.4,0.15));
#57669=CARTESIAN_POINT('',(-0.173205080756888,-0.64,-2.12115047744981E-17));
#57670=CARTESIAN_POINT('Origin',(0.0866025403784439,-0.4,0.15));
#57671=CARTESIAN_POINT('',(0.0866025403784439,-0.4,0.15));
#57672=CARTESIAN_POINT('',(-0.0866025403784439,-0.4,0.15));
#57673=CARTESIAN_POINT('',(0.0866025403784439,-0.64,0.15));
#57674=CARTESIAN_POINT('',(0.0866025403784439,-0.4,0.15));
#57675=CARTESIAN_POINT('',(-0.0866025403784439,-0.64,0.15));
#57676=CARTESIAN_POINT('Origin',(0.173205080756888,-0.4,0.));
#57677=CARTESIAN_POINT('',(0.0866025403784439,-0.4,0.15));
#57678=CARTESIAN_POINT('',(0.0866025403784439,-0.64,0.15));
#57679=CARTESIAN_POINT('Origin',(0.,-0.4,-2.77555756156289E-17));
#57680=CARTESIAN_POINT('Origin',(0.,-0.64,-2.77555756156289E-17));
#57681=CARTESIAN_POINT('Origin',(0.,-1.,0.));
#57682=CARTESIAN_POINT('',(-0.1954,-1.,2.39295984553393E-17));
#57683=CARTESIAN_POINT('Origin',(0.,-1.,0.));
#57684=CARTESIAN_POINT('Origin',(0.3,0.4,0.));
#57685=CARTESIAN_POINT('',(-0.3,0.4,-3.67394039744206E-17));
#57686=CARTESIAN_POINT('Origin',(0.,0.4,0.));
#57687=CARTESIAN_POINT('Origin',(0.,0.375,0.));
#57688=CARTESIAN_POINT('',(-0.35,0.35,-4.28626379701573E-17));
#57689=CARTESIAN_POINT('Origin',(0.,0.35,0.));
#57690=CARTESIAN_POINT('',(-0.325,0.375,-3.9801020972289E-17));
#57691=CARTESIAN_POINT('Origin',(0.,0.19,0.));
#57692=CARTESIAN_POINT('',(-0.35,0.03,-4.28626379701574E-17));
#57693=CARTESIAN_POINT('Origin',(0.,0.03,0.));
#57694=CARTESIAN_POINT('',(-0.35,0.19,-4.28626379701574E-17));
#57695=CARTESIAN_POINT('Origin',(0.,0.0149999999999999,0.));
#57696=CARTESIAN_POINT('',(-0.32,-3.29597460435593E-17,-3.91886975727153E-17));
#57697=CARTESIAN_POINT('Origin',(0.,0.,0.));
#57698=CARTESIAN_POINT('',(-0.335,0.0149999999999999,-4.10256677714363E-17));
#57699=CARTESIAN_POINT('Origin',(0.22,0.,0.));
#57700=CARTESIAN_POINT('',(-0.22,-6.93889390390723E-18,-2.69422295812418E-17));
#57701=CARTESIAN_POINT('Origin',(0.,0.,0.));
#57702=CARTESIAN_POINT('Origin',(0.,-0.02,0.));
#57703=CARTESIAN_POINT('',(-0.1954,-0.0492,2.39295984553393E-17));
#57704=CARTESIAN_POINT('Origin',(0.,-0.0492,0.));
#57705=CARTESIAN_POINT('',(-0.21,-0.02,-2.57175827820944E-17));
#57706=CARTESIAN_POINT('Origin',(0.,-0.8,0.));
#57707=CARTESIAN_POINT('',(-0.1954,-0.8,-2.39295984553393E-17));
#57840=UNCERTAINTY_MEASURE_WITH_UNIT(LENGTH_MEASURE(0.001),#57901,
'DISTANCE_ACCURACY_VALUE',
'Maximum model space distance between geometric entities at asserted c
onnectivities');
#57841=UNCERTAINTY_MEASURE_WITH_UNIT(LENGTH_MEASURE(0.001),#57901,
'DISTANCE_ACCURACY_VALUE',
'Maximum model space distance between geometric entities at asserted c
onnectivities');
#57899=(
GEOMETRIC_REPRESENTATION_CONTEXT(3)
GLOBAL_UNCERTAINTY_ASSIGNED_CONTEXT((#57840))
GLOBAL_UNIT_ASSIGNED_CONTEXT((#57901,#57903,#57904))
REPRESENTATION_CONTEXT('','3D')
);
#57900=(
GEOMETRIC_REPRESENTATION_CONTEXT(3)
GLOBAL_UNCERTAINTY_ASSIGNED_CONTEXT((#57841))
GLOBAL_UNIT_ASSIGNED_CONTEXT((#57901,#57903,#57904))
REPRESENTATION_CONTEXT('','3D')
);
#57901=(
LENGTH_UNIT()
NAMED_UNIT(*)
SI_UNIT(.CENTI.,.METRE.)
);
#57903=(
NAMED_UNIT(*)
PLANE_ANGLE_UNIT()
SI_UNIT($,.RADIAN.)
);
#57904=(
NAMED_UNIT(*)
SI_UNIT($,.STERADIAN.)
SOLID_ANGLE_UNIT()
);
#57962=SHAPE_DEFINITION_REPRESENTATION(#58033,#58166);
#58033=PRODUCT_DEFINITION_SHAPE('',$,#58225);
#58166=SHAPE_REPRESENTATION('',(#15479),#57899);
#58167=PRODUCT_DEFINITION_CONTEXT('part definition',#58343,'design');
#58225=PRODUCT_DEFINITION('M4x10 Cap Screw','M4x10 Cap Screw',#58283,#58167);
#58283=PRODUCT_DEFINITION_FORMATION('',$,#58402);
#58343=APPLICATION_CONTEXT(
'Core Data for Automotive Mechanical Design Process');
#58344=PRODUCT_CONTEXT('part definition',#58343,'mechanical');
#58402=PRODUCT('M4x10 Cap Screw','M4x10 Cap Screw','M4x10 Cap Screw',(#58344));
#58466=COLOUR_RGB('Black',0.12,0.14,0.17);
#58467=FILL_AREA_STYLE_COLOUR('',#58466);
#58468=FILL_AREA_STYLE('',(#58467));
#58469=SURFACE_STYLE_FILL_AREA(#58468);
#58470=SURFACE_SIDE_STYLE('',(#58469));
#58471=SURFACE_STYLE_USAGE(.BOTH.,#58470);
#58472=PRESENTATION_STYLE_ASSIGNMENT((#58471));
ENDSEC;
END-ISO-10303-21;
